ISO-10303-21;
HEADER;
FILE_DESCRIPTION (('STEP AP214'),
    '1' );
FILE_NAME ('socket button head screw_iso_ISO 7380 - M4 x 10 - 10N.step',
    '2026-10-24T08:20:21',
    ( '' ),
    ( '' ),
    'SwSTEP 2.0',
    'SolidWorks 2026',
    '' );
FILE_SCHEMA (( 'AUTOMOTIVE_DESIGN' ));
ENDSEC;

DATA;
#1=VERTEX_POINT ( 'NONE', #624 ) ;
#3=CARTESIAN_POINT ( 'NONE',  ( 1.300000000000000044, 1.443375672974065216, 7.222237291452134449E-31 ) ) ;
#9=DIRECTION ( 'NONE',  ( 0.000000000000000000, 0.000000000000000000, 1.000000000000000000 ) ) ;
#12=LINE ( 'NONE', #3823, #2390 ) ;
#19=DIRECTION ( 'NONE',  ( -0.7071067811865492381, 8.659560562354911904E-17, -0.7071067811865457964 ) ) ;
#23=LINE ( 'NONE', #2105, #2068 ) ;
#25=VECTOR ( 'NONE', #749, 1000.000000000000114 ) ;
#28=EDGE_LOOP ( 'NONE', ( #1681, #1312, #3374, #1579 ) ) ;
#31=EDGE_LOOP ( 'NONE', ( #3797, #723, #569, #2340, #3263 ) ) ;
#42=DIRECTION ( 'NONE',  ( 0.000000000000000000, 0.000000000000000000, 1.000000000000000000 ) ) ;
#44=DIRECTION ( 'NONE',  ( -0.000000000000000000, 0.5000000000000002220, -0.8660254037844384856 ) ) ;
#49=EDGE_CURVE ( 'NONE', #3210, #3147, #1369, .T. ) ;
#50=ORIENTED_EDGE ( 'NONE', *, *, #3736, .T. ) ;
#57=CARTESIAN_POINT ( 'NONE',  ( 2.200000000000000178, 0.000000000000000000, 3.799999999999999378 ) ) ;
#60=DIRECTION ( 'NONE',  ( 1.000000000000000000, 0.000000000000000000, -0.000000000000000000 ) ) ;
#67=ORIENTED_EDGE ( 'NONE', *, *, #1212, .F. ) ;
#69=FACE_OUTER_BOUND ( 'NONE', #2614, .T. ) ;
#71=AXIS2_PLACEMENT_3D ( 'NONE', #2197, #416, #1075 ) ;
#72=CARTESIAN_POINT ( 'NONE',  ( 1.300000000000000044, -0.7216878364870317197, -1.250000000000000000 ) ) ;
#84=DIRECTION ( 'NONE',  ( -1.000000000000000000, -0.000000000000000000, -0.000000000000000000 ) ) ;
#90=AXIS2_PLACEMENT_3D ( 'NONE', #3655, #2505, #3718 ) ;
#91=LINE ( 'NONE', #72, #1895 ) ;
#94=CARTESIAN_POINT ( 'NONE',  ( 0.000000000000000000, 0.000000000000000000, 1.999999999999999112 ) ) ;
#98=CARTESIAN_POINT ( 'NONE',  ( 1.300000000000000044, -0.7216878364870317197, -1.250000000000000000 ) ) ;
#104=FACE_OUTER_BOUND ( 'NONE', #1200, .T. ) ;
#109=DIRECTION ( 'NONE',  ( -1.000000000000000000, -0.000000000000000000, -0.000000000000000000 ) ) ;
#112=PLANE ( 'NONE',  #3812 ) ;
#113=ORIENTED_EDGE ( 'NONE', *, *, #1158, .T. ) ;
#120=CARTESIAN_POINT ( 'NONE',  ( 12.20000000000000107, 0.000000000000000000, 0.000000000000000000 ) ) ;
#124=LINE ( 'NONE', #2843, #702 ) ;
#126=CIRCLE ( 'NONE', #71, 1.999999999999999556 ) ;
#133=( GEOMETRIC_REPRESENTATION_CONTEXT ( 3 ) GLOBAL_UNCERTAINTY_ASSIGNED_CONTEXT ( ( #1987 ) ) GLOBAL_UNIT_ASSIGNED_CONTEXT ( ( #3301, #2413, #2158 ) ) REPRESENTATION_CONTEXT ( 'NONE', 'WORKASPACE' ) );
#134=EDGE_CURVE ( 'NONE', #1873, #2443, #3640, .T. ) ;
#137=VERTEX_POINT ( 'NONE', #2620 ) ;
#139=CIRCLE ( 'NONE', #3685, 1.250000000000000222 ) ;
#140=VECTOR ( 'NONE', #2256, 1000.000000000000000 ) ;
#146=DIRECTION ( 'NONE',  ( 0.000000000000000000, 0.8660254037844385966, -0.5000000000000003331 ) ) ;
#150=AXIS2_PLACEMENT_3D ( 'NONE', #3676, #1911, #3108 ) ;
#154=CIRCLE ( 'NONE', #90, 3.799999999999999378 ) ;
#169=CARTESIAN_POINT ( 'NONE',  ( 11.80999999999999872, 0.000000000000000000, 0.000000000000000000 ) ) ;
#172=ORIENTED_EDGE ( 'NONE', *, *, #567, .F. ) ;
#195=ORIENTED_EDGE ( 'NONE', *, *, #970, .T. ) ;
#196=EDGE_CURVE ( 'NONE', #673, #620, #3793, .T. ) ;
#212=PLANE ( 'NONE',  #3487 ) ;
#216=ORIENTED_EDGE ( 'NONE', *, *, #1379, .F. ) ;
#219=VECTOR ( 'NONE', #404, 1000.000000000000000 ) ;
#224=DIRECTION ( 'NONE',  ( 0.000000000000000000, -1.000000000000000000, 0.000000000000000000 ) ) ;
#226=ORIENTED_EDGE ( 'NONE', *, *, #2070, .F. ) ;
#229=SURFACE_STYLE_USAGE ( .BOTH. , #3555 ) ;
#232=LINE ( 'NONE', #2626, #1435 ) ;
#234=DIRECTION ( 'NONE',  ( -0.000000000000000000, -0.5000000000000002220, -0.8660254037844384856 ) ) ;
#235=ORIENTED_EDGE ( 'NONE', *, *, #2182, .F. ) ;
#239=ORIENTED_EDGE ( 'NONE', *, *, #1254, .T. ) ;
#244=( NAMED_UNIT ( * ) PLANE_ANGLE_UNIT ( ) SI_UNIT ( $, .RADIAN. ) );
#246=EDGE_LOOP ( 'NONE', ( #195, #3218 ) ) ;
#252=EDGE_LOOP ( 'NONE', ( #3787, #1790, #3683, #1738 ) ) ;
#257=STYLED_ITEM('',(#3881),#1995);
#260=SHAPE_DEFINITION_REPRESENTATION ( #1206, #556 ) ;
#281=ORIENTED_EDGE ( 'NONE', *, *, #3302, .F. ) ;
#283=VERTEX_POINT ( 'NONE', #3 ) ;
#284=DIRECTION ( 'NONE',  ( 1.000000000000000000, 0.000000000000000000, -0.000000000000000000 ) ) ;
#290=DIRECTION ( 'NONE',  ( 0.000000000000000000, 0.000000000000000000, 1.000000000000000000 ) ) ;
#300=EDGE_CURVE ( 'NONE', #3067, #2698, #472, .T. ) ;
#308=PLANE ( 'NONE',  #2884 ) ;
#310=CARTESIAN_POINT ( 'NONE',  ( 1.300000000000000044, -1.443375672974064328, 2.168404344971008868E-16 ) ) ;
#313=CARTESIAN_POINT ( 'NONE',  ( 0.000000000000000000, 0.000000000000000000, 0.000000000000000000 ) ) ;
#319=MECHANICAL_DESIGN_GEOMETRIC_PRESENTATION_REPRESENTATION('',(#257),#133);
#324=TOROIDAL_SURFACE ( 'NONE', #959, 2.199999999999999289, 0.2000000000000000111 ) ;
#330=ORIENTED_EDGE ( 'NONE', *, *, #196, .T. ) ;
#331=CIRCLE ( 'NONE', #3200, 1.999999999999999556 ) ;
#333=CIRCLE ( 'NONE', #2451, 0.2000000000000000944 ) ;
#334=AXIS2_PLACEMENT_3D ( 'NONE', #344, #1188, #42 ) ;
#336=ORIENTED_EDGE ( 'NONE', *, *, #3302, .T. ) ;
#344=CARTESIAN_POINT ( 'NONE',  ( 1.820000000000000062, 0.000000000000000000, 0.000000000000000000 ) ) ;
#352=CARTESIAN_POINT ( 'NONE',  ( 2.399999999999999911, 0.000000000000000000, 0.000000000000000000 ) ) ;
#354=DIRECTION ( 'NONE',  ( -1.000000000000000000, -0.000000000000000000, -0.000000000000000000 ) ) ;
#357=DIRECTION ( 'NONE',  ( -1.000000000000000000, -0.000000000000000000, -0.000000000000000000 ) ) ;
#362=CYLINDRICAL_SURFACE ( 'NONE', #3771, 3.799999999999999378 ) ;
#366=ORIENTED_EDGE ( 'NONE', *, *, #3600, .F. ) ;
#367=DIRECTION ( 'NONE',  ( 0.000000000000000000, 0.000000000000000000, 1.000000000000000000 ) ) ;
#374=AXIS2_PLACEMENT_3D ( 'NONE', #1676, #2860, #3740 ) ;
#380=FACE_OUTER_BOUND ( 'NONE', #736, .T. ) ;
#383=VECTOR ( 'NONE', #950, 1000.000000000000114 ) ;
#384=ORIENTED_EDGE ( 'NONE', *, *, #802, .F. ) ;
#395=CARTESIAN_POINT ( 'NONE',  ( 0.000000000000000000, 2.449293598294705428E-16, -1.999999999999999112 ) ) ;
#404=DIRECTION ( 'NONE',  ( -1.000000000000000000, -0.000000000000000000, -0.000000000000000000 ) ) ;
#409=DIRECTION ( 'NONE',  ( 1.000000000000000000, 0.000000000000000000, -0.000000000000000000 ) ) ;
#416=DIRECTION ( 'NONE',  ( -1.000000000000000000, -0.000000000000000000, -0.000000000000000000 ) ) ;
#426=SPHERICAL_SURFACE ( 'NONE', #1328, 4.324969328314201000 ) ;
#431=ADVANCED_FACE ( 'NONE', ( #104 ), #2236, .T. ) ;
#439=ADVANCED_FACE ( 'NONE', ( #3382, #69 ), #3691, .F. ) ;
#440=DIRECTION ( 'NONE',  ( 0.000000000000000000, 1.224646799147353207E-16, -1.000000000000000000 ) ) ;
#450=AXIS2_PLACEMENT_3D ( 'NONE', #3093, #409, #1599 ) ;
#455=DIRECTION ( 'NONE',  ( -1.000000000000000000, -0.000000000000000000, -0.000000000000000000 ) ) ;
#463=AXIS2_PLACEMENT_3D ( 'NONE', #3102, #1058, #3695 ) ;
#472=CIRCLE ( 'NONE', #1713, 1.999999999999999112 ) ;
#474=CARTESIAN_POINT ( 'NONE',  ( 1.300000000000000044, 0.7216878364870329410, -1.250000000000000000 ) ) ;
#492=ADVANCED_FACE ( 'NONE', ( #3403 ), #2773, .T. ) ;
#497=ORIENTED_EDGE ( 'NONE', *, *, #2033, .T. ) ;
#507=EDGE_CURVE ( 'NONE', #620, #2556, #2157, .T. ) ;
#511=VERTEX_POINT ( 'NONE', #694 ) ;
#524=ORIENTED_EDGE ( 'NONE', *, *, #3730, .F. ) ;
#527=AXIS2_PLACEMENT_3D ( 'NONE', #922, #2066, #1791 ) ;
#529=EDGE_LOOP ( 'NONE', ( #1931, #3571, #1260, #616, #3835 ) ) ;
#532=AXIS2_PLACEMENT_3D ( 'NONE', #3160, #1989, #3703 ) ;
#543=ORIENTED_EDGE ( 'NONE', *, *, #1379, .T. ) ;
#549=EDGE_CURVE ( 'NONE', #1148, #2170, #2172, .T. ) ;
#552=ORIENTED_EDGE ( 'NONE', *, *, #835, .F. ) ;
#555=ADVANCED_FACE ( 'NONE', ( #1010 ), #2255, .T. ) ;
#556=SHAPE_REPRESENTATION ( 'socket button head screw_iso_ISO 7380 - M4 x 10 - 10N', ( #2207 ), #1040 ) ;
#560=CARTESIAN_POINT ( 'NONE',  ( 11.80999999999999872, 0.000000000000000000, 1.999999999999999556 ) ) ;
#562=EDGE_CURVE ( 'NONE', #1255, #1889, #331, .T. ) ;
#564=EDGE_CURVE ( 'NONE', #1187, #929, #2020, .T. ) ;
#567=EDGE_CURVE ( 'NONE', #2170, #2092, #1335, .T. ) ;
#568=DIRECTION ( 'NONE',  ( -0.000000000000000000, 0.5000000000000000000, 0.8660254037844385966 ) ) ;
#569=ORIENTED_EDGE ( 'NONE', *, *, #3600, .T. ) ;
#570=CIRCLE ( 'NONE', #374, 3.799999999999999378 ) ;
#586=CARTESIAN_POINT ( 'NONE',  ( 0.000000000000000000, 0.7216878364870329410, -1.250000000000000000 ) ) ;
#587=VECTOR ( 'NONE', #2366, 1000.000000000000114 ) ;
#588=CARTESIAN_POINT ( 'NONE',  ( 1.300000000000000044, -1.443375672974064328, 1.278502688459867223E-18 ) ) ;
#596=ORIENTED_EDGE ( 'NONE', *, *, #300, .T. ) ;
#602=LINE ( 'NONE', #2115, #383 ) ;
#604=EDGE_CURVE ( 'NONE', #964, #511, #1830, .T. ) ;
#607=DIRECTION ( 'NONE',  ( 1.000000000000000000, 0.000000000000000000, -0.000000000000000000 ) ) ;
#608=ADVANCED_FACE ( 'NONE', ( #1475 ), #848, .T. ) ;
#612=EDGE_CURVE ( 'NONE', #2092, #1136, #2029, .T. ) ;
#614=FACE_OUTER_BOUND ( 'NONE', #2550, .T. ) ;
#616=ORIENTED_EDGE ( 'NONE', *, *, #507, .F. ) ;
#620=VERTEX_POINT ( 'NONE', #956 ) ;
#624=CARTESIAN_POINT ( 'NONE',  ( 1.300000000000000044, 1.082531754730548856, -0.6250000000000002220 ) ) ;
#631=FACE_OUTER_BOUND ( 'NONE', #28, .T. ) ;
#632=VECTOR ( 'NONE', #1734, 1000.000000000000000 ) ;
#634=CYLINDRICAL_SURFACE ( 'NONE', #3503, 1.999999999999999112 ) ;
#635=DIRECTION ( 'NONE',  ( 1.000000000000000000, 0.000000000000000000, 0.000000000000000000 ) ) ;
#639=VECTOR ( 'NONE', #2886, 1000.000000000000000 ) ;
#643=AXIS2_PLACEMENT_3D ( 'NONE', #1477, #2403, #9 ) ;
#666=CARTESIAN_POINT ( 'NONE',  ( 1.300000000000000044, -1.082531754730548190, 0.6250000000000002220 ) ) ;
#667=EDGE_CURVE ( 'NONE', #1, #283, #3269, .T. ) ;
#673=VERTEX_POINT ( 'NONE', #1773 ) ;
#677=CARTESIAN_POINT ( 'NONE',  ( 1.300000000000000044, -0.7216878364870317197, 1.250000000000000000 ) ) ;
#683=LINE ( 'NONE', #1271, #2694 ) ;
#684=EDGE_CURVE ( 'NONE', #1516, #929, #1247, .T. ) ;
#689=DIRECTION ( 'NONE',  ( 0.000000000000000000, 0.000000000000000000, 1.000000000000000000 ) ) ;
#691=VERTEX_POINT ( 'NONE', #1455 ) ;
#694=CARTESIAN_POINT ( 'NONE',  ( 0.000000000000000000, 0.7216878364870329410, -1.250000000000000000 ) ) ;
#702=VECTOR ( 'NONE', #3081, 1000.000000000000227 ) ;
#711=ORIENTED_EDGE ( 'NONE', *, *, #300, .F. ) ;
#719=EDGE_CURVE ( 'NONE', #2633, #964, #91, .T. ) ;
#723=ORIENTED_EDGE ( 'NONE', *, *, #612, .T. ) ;
#726=VECTOR ( 'NONE', #1249, 1000.000000000000000 ) ;
#736=EDGE_LOOP ( 'NONE', ( #3178, #3153, #1073, #2475, #172 ) ) ;
#738=CARTESIAN_POINT ( 'NONE',  ( 0.000000000000000000, -0.7216878364870317197, 1.250000000000000000 ) ) ;
#745=DIRECTION ( 'NONE',  ( -0.000000000000000000, 1.000000000000000000, 1.224646799147353207E-16 ) ) ;
#749=DIRECTION ( 'NONE',  ( -0.000000000000000000, 0.5000000000000002220, -0.8660254037844384856 ) ) ;
#762=CARTESIAN_POINT ( 'NONE',  ( 3.885274725274725949, -4.336808689942017736E-16, 0.000000000000000000 ) ) ;
#766=EDGE_LOOP ( 'NONE', ( #2477, #3283 ) ) ;
#768=EDGE_LOOP ( 'NONE', ( #336, #812, #1881, #3232, #2122 ) ) ;
#778=ORIENTED_EDGE ( 'NONE', *, *, #3778, .T. ) ;
#781=APPLICATION_CONTEXT ( 'automotive_design' ) ;
#787=PLANE ( 'NONE',  #1344 ) ;
#798=DIRECTION ( 'NONE',  ( -0.000000000000000000, 0.5000000000000002220, -0.8660254037844384856 ) ) ;
#802=EDGE_CURVE ( 'NONE', #1148, #2036, #154, .T. ) ;
#804=EDGE_CURVE ( 'NONE', #1813, #2443, #2339, .T. ) ;
#807=ORIENTED_EDGE ( 'NONE', *, *, #3136, .F. ) ;
#808=EDGE_CURVE ( 'NONE', #283, #1408, #2240, .T. ) ;
#812=ORIENTED_EDGE ( 'NONE', *, *, #1575, .T. ) ;
#814=DIRECTION ( 'NONE',  ( 0.000000000000000000, 0.000000000000000000, 1.000000000000000000 ) ) ;
#820=CARTESIAN_POINT ( 'NONE',  ( 0.000000000000000000, 0.000000000000000000, 0.000000000000000000 ) ) ;
#835=EDGE_CURVE ( 'NONE', #929, #1729, #1301, .T. ) ;
#847=COLOUR_RGB ( '',1.000000000000000000, 0.9490196078431372140, 0.9098039215686274384 ) ;
#848=CONICAL_SURFACE ( 'NONE', #1963, 1.610000000000000098, 0.7853981633974458365 ) ;
#859=DIRECTION ( 'NONE',  ( 0.000000000000000000, -1.502314598737159031E-16, -1.000000000000000000 ) ) ;
#865=( NAMED_UNIT ( * ) SI_UNIT ( $, .STERADIAN. ) SOLID_ANGLE_UNIT ( ) );
#872=LINE ( 'NONE', #3231, #2503 ) ;
#873=ORIENTED_EDGE ( 'NONE', *, *, #2182, .T. ) ;
#888=ORIENTED_EDGE ( 'NONE', *, *, #808, .T. ) ;
#889=CARTESIAN_POINT ( 'NONE',  ( 12.20000000000000107, 2.210487472460972205E-16, -1.610000000000000098 ) ) ;
#895=AXIS2_PLACEMENT_3D ( 'NONE', #1164, #859, #1728 ) ;
#896=ORIENTED_EDGE ( 'NONE', *, *, #134, .T. ) ;
#898=( NAMED_UNIT ( * ) SI_UNIT ( $, .STERADIAN. ) SOLID_ANGLE_UNIT ( ) );
#904=DIRECTION ( 'NONE',  ( 0.000000000000000000, 0.000000000000000000, 1.000000000000000000 ) ) ;
#917=CARTESIAN_POINT ( 'NONE',  ( 1.300000000000000044, -1.443375672974064328, 2.168404344971008868E-16 ) ) ;
#922=CARTESIAN_POINT ( 'NONE',  ( 1.820000000000000062, 0.000000000000000000, 0.000000000000000000 ) ) ;
#925=DIRECTION ( 'NONE',  ( 0.000000000000000000, 0.000000000000000000, 1.000000000000000000 ) ) ;
#929=VERTEX_POINT ( 'NONE', #1646 ) ;
#931=CARTESIAN_POINT ( 'NONE',  ( 8.673617379884035472E-16, 0.000000000000000000, 0.000000000000000000 ) ) ;
#932=EDGE_LOOP ( 'NONE', ( #2133, #2546, #3592, #3528, #1761, #330 ) ) ;
#944=ORIENTED_EDGE ( 'NONE', *, *, #1158, .F. ) ;
#946=ORIENTED_EDGE ( 'NONE', *, *, #1525, .F. ) ;
#949=EDGE_LOOP ( 'NONE', ( #1236, #873, #1842, #2456 ) ) ;
#950=DIRECTION ( 'NONE',  ( -0.5000000000000042188, 1.060575238724903710E-16, -0.8660254037844361541 ) ) ;
#956=CARTESIAN_POINT ( 'NONE',  ( 0.000000000000000000, 0.7216878364870329410, 1.249999999999999778 ) ) ;
#959=AXIS2_PLACEMENT_3D ( 'NONE', #3710, #1932, #367 ) ;
#964=VERTEX_POINT ( 'NONE', #1919 ) ;
#970=EDGE_CURVE ( 'NONE', #2875, #2365, #2767, .T. ) ;
#1006=FACE_OUTER_BOUND ( 'NONE', #3126, .T. ) ;
#1010=FACE_OUTER_BOUND ( 'NONE', #3073, .T. ) ;
#1019=VECTOR ( 'NONE', #2726, 1000.000000000000114 ) ;
#1020=DIRECTION ( 'NONE',  ( 0.000000000000000000, 0.000000000000000000, 1.000000000000000000 ) ) ;
#1023=AXIS2_PLACEMENT_3D ( 'NONE', #917, #284, #2703 ) ;
#1032=AXIS2_PLACEMENT_3D ( 'NONE', #1070, #2548, #3734 ) ;
#1040=( GEOMETRIC_REPRESENTATION_CONTEXT ( 3 ) GLOBAL_UNCERTAINTY_ASSIGNED_CONTEXT ( ( #1958 ) ) GLOBAL_UNIT_ASSIGNED_CONTEXT ( ( #3266, #244, #865 ) ) REPRESENTATION_CONTEXT ( 'NONE', 'WORKASPACE' ) );
#1051=EDGE_CURVE ( 'NONE', #1495, #691, #2285, .T. ) ;
#1055=CARTESIAN_POINT ( 'NONE',  ( 2.199999999999999734, 0.000000000000000000, 0.000000000000000000 ) ) ;
#1057=LINE ( 'NONE', #395, #3563 ) ;
#1058=DIRECTION ( 'NONE',  ( 0.000000000000000000, 0.000000000000000000, 1.000000000000000000 ) ) ;
#1062=DIRECTION ( 'NONE',  ( -0.000000000000000000, 0.000000000000000000, -1.000000000000000000 ) ) ;
#1064=ORIENTED_EDGE ( 'NONE', *, *, #2379, .F. ) ;
#1070=CARTESIAN_POINT ( 'NONE',  ( 0.000000000000000000, 0.000000000000000000, 0.000000000000000000 ) ) ;
#1073=ORIENTED_EDGE ( 'NONE', *, *, #1212, .T. ) ;
#1075=DIRECTION ( 'NONE',  ( 0.000000000000000000, 0.000000000000000000, 1.000000000000000000 ) ) ;
#1086=AXIS2_PLACEMENT_3D ( 'NONE', #2752, #84, #689 ) ;
#1092=EDGE_CURVE ( 'NONE', #2875, #3067, #2650, .T. ) ;
#1096=CARTESIAN_POINT ( 'NONE',  ( 1.820000000000000062, 3.799999999999999378, 0.000000000000000000 ) ) ;
#1136=VERTEX_POINT ( 'NONE', #1376 ) ;
#1139=CIRCLE ( 'NONE', #3191, 1.250000000000000222 ) ;
#1148=VERTEX_POINT ( 'NONE', #1413 ) ;
#1156=DIRECTION ( 'NONE',  ( -1.000000000000000000, -0.000000000000000000, -0.000000000000000000 ) ) ;
#1158=EDGE_CURVE ( 'NONE', #283, #673, #2601, .T. ) ;
#1164=CARTESIAN_POINT ( 'NONE',  ( 1.300000000000000044, -0.7216878364870317197, 1.250000000000000000 ) ) ;
#1168=CARTESIAN_POINT ( 'NONE',  ( 8.673617379884035472E-16, -1.899999999999999689, -3.490243377569955568E-16 ) ) ;
#1171=DIRECTION ( 'NONE',  ( -0.000000000000000000, 0.000000000000000000, -1.000000000000000000 ) ) ;
#1183=CARTESIAN_POINT ( 'NONE',  ( 0.000000000000000000, 0.000000000000000000, 0.000000000000000000 ) ) ;
#1187=VERTEX_POINT ( 'NONE', #666 ) ;
#1188=DIRECTION ( 'NONE',  ( -1.000000000000000000, -0.000000000000000000, -0.000000000000000000 ) ) ;
#1191=ORIENTED_EDGE ( 'NONE', *, *, #3705, .T. ) ;
#1197=AXIS2_PLACEMENT_3D ( 'NONE', #352, #1219, #2421 ) ;
#1200=EDGE_LOOP ( 'NONE', ( #1307, #497, #50, #2776, #2114 ) ) ;
#1206=PRODUCT_DEFINITION_SHAPE ( 'NONE', 'NONE',  #3366 ) ;
#1208=ORIENTED_EDGE ( 'NONE', *, *, #3166, .F. ) ;
#1212=EDGE_CURVE ( 'NONE', #2036, #1136, #2120, .T. ) ;
#1219=DIRECTION ( 'NONE',  ( -1.000000000000000000, -0.000000000000000000, -0.000000000000000000 ) ) ;
#1225=DIRECTION ( 'NONE',  ( -1.000000000000000000, -0.000000000000000000, -0.000000000000000000 ) ) ;
#1236=ORIENTED_EDGE ( 'NONE', *, *, #1776, .T. ) ;
#1247=LINE ( 'NONE', #3248, #3767 ) ;
#1249=DIRECTION ( 'NONE',  ( -1.000000000000000000, -0.000000000000000000, -0.000000000000000000 ) ) ;
#1250=DIRECTION ( 'NONE',  ( 0.000000000000000000, 0.5000000000000001110, -0.8660254037844385966 ) ) ;
#1252=ADVANCED_FACE ( 'NONE', ( #380 ), #362, .T. ) ;
#1254=EDGE_CURVE ( 'NONE', #1889, #3067, #1834, .T. ) ;
#1255=VERTEX_POINT ( 'NONE', #1288 ) ;
#1260=ORIENTED_EDGE ( 'NONE', *, *, #1698, .T. ) ;
#1263=LINE ( 'NONE', #3347, #2938 ) ;
#1268=AXIS2_PLACEMENT_3D ( 'NONE', #310, #2992, #1500 ) ;
#1271=CARTESIAN_POINT ( 'NONE',  ( 1.300000000000000044, 0.7216878364870329410, 1.249999999999999778 ) ) ;
#1287=CARTESIAN_POINT ( 'NONE',  ( 4.336808689942017736E-16, 0.000000000000000000, 0.000000000000000000 ) ) ;
#1288=CARTESIAN_POINT ( 'NONE',  ( 11.80999999999999872, 2.449293598294705921E-16, -1.999999999999999556 ) ) ;
#1290=ADVANCED_FACE ( 'NONE', ( #3603 ), #3028, .F. ) ;
#1294=PLANE ( 'NONE',  #450 ) ;
#1296=CARTESIAN_POINT ( 'NONE',  ( 2.199999999999999734, 0.000000000000000000, 2.199999999999999289 ) ) ;
#1301=LINE ( 'NONE', #677, #3821 ) ;
#1303=DIRECTION ( 'NONE',  ( 0.000000000000000000, 0.000000000000000000, 1.000000000000000000 ) ) ;
#1304=ADVANCED_FACE ( 'NONE', ( #1386 ), #2554, .T. ) ;
#1307=ORIENTED_EDGE ( 'NONE', *, *, #3136, .T. ) ;
#1312=ORIENTED_EDGE ( 'NONE', *, *, #970, .F. ) ;
#1314=CARTESIAN_POINT ( 'NONE',  ( 1.300000000000000044, 0.7216878364870329410, -1.250000000000000000 ) ) ;
#1319=FACE_OUTER_BOUND ( 'NONE', #3009, .T. ) ;
#1324=VECTOR ( 'NONE', #798, 1000.000000000000114 ) ;
#1327=EDGE_CURVE ( 'NONE', #1, #1495, #2210, .T. ) ;
#1328=AXIS2_PLACEMENT_3D ( 'NONE', #1585, #2545, #2479 ) ;
#1335=CIRCLE ( 'NONE', #527, 3.799999999999999378 ) ;
#1344=AXIS2_PLACEMENT_3D ( 'NONE', #2537, #3428, #2224 ) ;
#1346=VERTEX_POINT ( 'NONE', #1927 ) ;
#1347=PRODUCT_CONTEXT ( 'NONE', #781, 'mechanical' ) ;
#1349=DIRECTION ( 'NONE',  ( 0.000000000000000000, -0.5000000000000000000, -0.8660254037844385966 ) ) ;
#1360=ADVANCED_FACE ( 'NONE', ( #1612 ), #787, .T. ) ;
#1366=ORIENTED_EDGE ( 'NONE', *, *, #2311, .F. ) ;
#1369=CIRCLE ( 'NONE', #1684, 1.610000000000000098 ) ;
#1376=CARTESIAN_POINT ( 'NONE',  ( 1.820000000000000062, 0.000000000000000000, 3.799999999999999378 ) ) ;
#1379=EDGE_CURVE ( 'NONE', #929, #1408, #2496, .T. ) ;
#1386=FACE_OUTER_BOUND ( 'NONE', #2322, .T. ) ;
#1405=FACE_OUTER_BOUND ( 'NONE', #768, .T. ) ;
#1408=VERTEX_POINT ( 'NONE', #2882 ) ;
#1410=EDGE_CURVE ( 'NONE', #2092, #1873, #1871, .T. ) ;
#1413=CARTESIAN_POINT ( 'NONE',  ( 2.200000000000000178, 4.653657836759941744E-16, -3.799999999999999378 ) ) ;
#1414=CARTESIAN_POINT ( 'NONE',  ( 0.000000000000000000, -0.7216878364870317197, -1.250000000000000000 ) ) ;
#1420=CARTESIAN_POINT ( 'NONE',  ( 12.20000000000000107, 0.000000000000000000, 1.610000000000000098 ) ) ;
#1422=ADVANCED_FACE ( 'NONE', ( #2512 ), #1910, .F. ) ;
#1424=ORIENTED_EDGE ( 'NONE', *, *, #2738, .T. ) ;
#1426=ORIENTED_EDGE ( 'NONE', *, *, #2738, .F. ) ;
#1435=VECTOR ( 'NONE', #2049, 1000.000000000000000 ) ;
#1453=PRESENTATION_STYLE_ASSIGNMENT (( #229 ) ) ;
#1455=CARTESIAN_POINT ( 'NONE',  ( 1.300000000000000044, -1.082531754730548412, -0.6250000000000003331 ) ) ;
#1464=EDGE_LOOP ( 'NONE', ( #235, #3768, #239, #596 ) ) ;
#1465=DIRECTION ( 'NONE',  ( -1.000000000000000000, 0.000000000000000000, -0.000000000000000000 ) ) ;
#1474=ORIENTED_EDGE ( 'NONE', *, *, #1626, .F. ) ;
#1475=FACE_OUTER_BOUND ( 'NONE', #252, .T. ) ;
#1477=CARTESIAN_POINT ( 'NONE',  ( 12.20000000000000107, 0.000000000000000000, 0.000000000000000000 ) ) ;
#1479=ORIENTED_EDGE ( 'NONE', *, *, #2634, .F. ) ;
#1481=CARTESIAN_POINT ( 'NONE',  ( 12.20000000000000107, 0.000000000000000000, 1.610000000000000098 ) ) ;
#1483=DIRECTION ( 'NONE',  ( -1.000000000000000000, 0.000000000000000000, 0.000000000000000000 ) ) ;
#1488=ADVANCED_FACE ( 'NONE', ( #2342 ), #2942, .F. ) ;
#1495=VERTEX_POINT ( 'NONE', #2032 ) ;
#1498=DIRECTION ( 'NONE',  ( -0.000000000000000000, 0.000000000000000000, 1.000000000000000000 ) ) ;
#1500=DIRECTION ( 'NONE',  ( -0.000000000000000000, 0.000000000000000000, -1.000000000000000000 ) ) ;
#1504=ORIENTED_EDGE ( 'NONE', *, *, #3613, .T. ) ;
#1505=FACE_OUTER_BOUND ( 'NONE', #3214, .T. ) ;
#1510=DIRECTION ( 'NONE',  ( -1.000000000000000000, -0.000000000000000000, -0.000000000000000000 ) ) ;
#1516=VERTEX_POINT ( 'NONE', #3798 ) ;
#1525=EDGE_CURVE ( 'NONE', #3210, #1889, #3541, .T. ) ;
#1528=VERTEX_POINT ( 'NONE', #588 ) ;
#1531=CARTESIAN_POINT ( 'NONE',  ( 1.300000000000000044, -1.443375672974064328, 1.278502688459867223E-18 ) ) ;
#1535=ADVANCED_FACE ( 'NONE', ( #1405 ), #212, .T. ) ;
#1538=DIRECTION ( 'NONE',  ( -1.000000000000000000, 0.000000000000000000, 0.000000000000000000 ) ) ;
#1545=LINE ( 'NONE', #2737, #1946 ) ;
#1551=LINE ( 'NONE', #2139, #2004 ) ;
#1553=CARTESIAN_POINT ( 'NONE',  ( 0.000000000000000000, 0.000000000000000000, 0.000000000000000000 ) ) ;
#1555=ORIENTED_EDGE ( 'NONE', *, *, #2618, .F. ) ;
#1559=AXIS2_PLACEMENT_3D ( 'NONE', #1287, #3305, #2689 ) ;
#1570=AXIS2_PLACEMENT_3D ( 'NONE', #313, #2724, #2370 ) ;
#1575=EDGE_CURVE ( 'NONE', #1495, #137, #232, .T. ) ;
#1579=ORIENTED_EDGE ( 'NONE', *, *, #2292, .F. ) ;
#1583=MECHANICAL_DESIGN_GEOMETRIC_PRESENTATION_REPRESENTATION('',(#1651),#2089);
#1585=CARTESIAN_POINT ( 'NONE',  ( 3.885274725274725949, -4.336808689942017736E-16, 0.000000000000000000 ) ) ;
#1590=AXIS2_PLACEMENT_3D ( 'NONE', #2501, #2529, #1903 ) ;
#1599=DIRECTION ( 'NONE',  ( -0.000000000000000000, 0.000000000000000000, -1.000000000000000000 ) ) ;
#1601=ORIENTED_EDGE ( 'NONE', *, *, #2388, .T. ) ;
#1605=ADVANCED_FACE ( 'NONE', ( #2119, #2709 ), #2729, .T. ) ;
#1612=FACE_OUTER_BOUND ( 'NONE', #3605, .T. ) ;
#1613=CARTESIAN_POINT ( 'NONE',  ( 1.300000000000000044, -1.443375672974064328, 1.278502688459867223E-18 ) ) ;
#1616=ORIENTED_EDGE ( 'NONE', *, *, #804, .F. ) ;
#1620=SPHERICAL_SURFACE ( 'NONE', #2881, 4.324969328314201000 ) ;
#1624=DIRECTION ( 'NONE',  ( -1.000000000000000000, -0.000000000000000000, -0.000000000000000000 ) ) ;
#1626=EDGE_CURVE ( 'NONE', #1528, #691, #23, .T. ) ;
#1629=ORIENTED_EDGE ( 'NONE', *, *, #2634, .T. ) ;
#1635=CARTESIAN_POINT ( 'NONE',  ( 1.300000000000000044, -1.443375672974064328, 2.168404344971008868E-16 ) ) ;
#1646=CARTESIAN_POINT ( 'NONE',  ( 1.300000000000000044, 1.877893248421448789E-16, 1.250000000000000000 ) ) ;
#1648=VECTOR ( 'NONE', #3079, 1000.000000000000000 ) ;
#1650=LINE ( 'NONE', #1314, #140 ) ;
#1651=STYLED_ITEM ( 'NONE', ( #1453 ), #2870 ) ;
#1665=CARTESIAN_POINT ( 'NONE',  ( 0.000000000000000000, -1.443375672974064328, 1.278502688459867223E-18 ) ) ;
#1668=DIRECTION ( 'NONE',  ( 0.000000000000000000, 0.000000000000000000, 1.000000000000000000 ) ) ;
#1673=DIRECTION ( 'NONE',  ( -1.000000000000000000, -0.000000000000000000, -0.000000000000000000 ) ) ;
#1676=CARTESIAN_POINT ( 'NONE',  ( 2.200000000000000178, 0.000000000000000000, 0.000000000000000000 ) ) ;
#1677=FILL_AREA_STYLE_COLOUR ( '', #847 ) ;
#1681=ORIENTED_EDGE ( 'NONE', *, *, #3778, .F. ) ;
#1684=AXIS2_PLACEMENT_3D ( 'NONE', #3423, #2935, #3739 ) ;
#1685=PRODUCT_DEFINITION_CONTEXT ( 'detailed design', #3101, 'design' ) ;
#1688=CARTESIAN_POINT ( 'NONE',  ( 1.300000000000000044, 1.443375672974065216, 7.222237291452134449E-31 ) ) ;
#1698=EDGE_CURVE ( 'NONE', #1729, #2556, #1551, .T. ) ;
#1707=TOROIDAL_SURFACE ( 'NONE', #1197, 2.199999999999999289, 0.2000000000000000111 ) ;
#1713=AXIS2_PLACEMENT_3D ( 'NONE', #2356, #635, #3581 ) ;
#1717=VECTOR ( 'NONE', #2983, 1000.000000000000227 ) ;
#1719=AXIS2_PLACEMENT_3D ( 'NONE', #2245, #2267, #1349 ) ;
#1728=DIRECTION ( 'NONE',  ( 0.000000000000000000, 1.000000000000000000, -1.502314598737159031E-16 ) ) ;
#1729=VERTEX_POINT ( 'NONE', #3349 ) ;
#1730=CARTESIAN_POINT ( 'NONE',  ( 0.000000000000000000, 0.7216878364870329410, 1.249999999999999778 ) ) ;
#1734=DIRECTION ( 'NONE',  ( -0.7071067811865492381, 0.000000000000000000, 0.7071067811865457964 ) ) ;
#1738=ORIENTED_EDGE ( 'NONE', *, *, #562, .F. ) ;
#1739=CARTESIAN_POINT ( 'NONE',  ( 2.399999999999999911, 0.000000000000000000, 1.999999999999999112 ) ) ;
#1757=CIRCLE ( 'NONE', #2264, 1.999999999999999112 ) ;
#1761=ORIENTED_EDGE ( 'NONE', *, *, #1827, .T. ) ;
#1771=VECTOR ( 'NONE', #2814, 1000.000000000000000 ) ;
#1773=CARTESIAN_POINT ( 'NONE',  ( 0.000000000000000000, 1.443375672974065216, 7.222237291452134449E-31 ) ) ;
#1775=AXIS2_PLACEMENT_3D ( 'NONE', #1055, #2235, #3690 ) ;
#1776=EDGE_CURVE ( 'NONE', #1889, #1255, #126, .T. ) ;
#1785=EDGE_CURVE ( 'NONE', #2036, #1148, #570, .T. ) ;
#1787=ORIENTED_EDGE ( 'NONE', *, *, #684, .F. ) ;
#1790=ORIENTED_EDGE ( 'NONE', *, *, #3606, .T. ) ;
#1791=DIRECTION ( 'NONE',  ( 0.000000000000000000, 0.000000000000000000, 1.000000000000000000 ) ) ;
#1795=PRODUCT ( 'socket button head screw_iso_ISO 7380 - M4 x 10 - 10N', 'socket button head screw_iso_ISO 7380 - M4 x 10 - 10N', '', ( #1347 ) ) ;
#1800=PLANE ( 'NONE',  #1268 ) ;
#1802=CARTESIAN_POINT ( 'NONE',  ( 2.399999999999999911, 2.449293598294705428E-16, -1.999999999999999112 ) ) ;
#1813=VERTEX_POINT ( 'NONE', #1096 ) ;
#1816=ORIENTED_EDGE ( 'NONE', *, *, #3736, .F. ) ;
#1825=PLANE ( 'NONE',  #1023 ) ;
#1827=EDGE_CURVE ( 'NONE', #511, #673, #124, .T. ) ;
#1830=LINE ( 'NONE', #586, #3698 ) ;
#1834=LINE ( 'NONE', #94, #726 ) ;
#1842=ORIENTED_EDGE ( 'NONE', *, *, #2292, .T. ) ;
#1846=ADVANCED_FACE ( 'NONE', ( #1319 ), #2378, .F. ) ;
#1853=LINE ( 'NONE', #474, #639 ) ;
#1865=DIRECTION ( 'NONE',  ( 0.000000000000000000, -0.8660254037844385966, -0.5000000000000001110 ) ) ;
#1867=ORIENTED_EDGE ( 'NONE', *, *, #2070, .T. ) ;
#1871=CIRCLE ( 'NONE', #3064, 4.324969328314200112 ) ;
#1873=VERTEX_POINT ( 'NONE', #1168 ) ;
#1876=DIRECTION ( 'NONE',  ( -1.000000000000000000, -0.000000000000000000, -0.000000000000000000 ) ) ;
#1881=ORIENTED_EDGE ( 'NONE', *, *, #2153, .T. ) ;
#1888=AXIS2_PLACEMENT_3D ( 'NONE', #120, #357, #1920 ) ;
#1889=VERTEX_POINT ( 'NONE', #560 ) ;
#1895=VECTOR ( 'NONE', #3405, 1000.000000000000000 ) ;
#1903=DIRECTION ( 'NONE',  ( -0.000000000000000000, 0.000000000000000000, 1.000000000000000000 ) ) ;
#1910=PLANE ( 'NONE',  #2257 ) ;
#1911=DIRECTION ( 'NONE',  ( -1.000000000000000000, -0.000000000000000000, -0.000000000000000000 ) ) ;
#1914=ORIENTED_EDGE ( 'NONE', *, *, #567, .T. ) ;
#1919=CARTESIAN_POINT ( 'NONE',  ( 0.000000000000000000, -0.7216878364870317197, -1.250000000000000000 ) ) ;
#1920=DIRECTION ( 'NONE',  ( 0.000000000000000000, 0.000000000000000000, 1.000000000000000000 ) ) ;
#1927=CARTESIAN_POINT ( 'NONE',  ( 1.300000000000000044, 0.7216878364870329410, 1.249999999999999778 ) ) ;
#1931=ORIENTED_EDGE ( 'NONE', *, *, #3166, .T. ) ;
#1932=DIRECTION ( 'NONE',  ( -1.000000000000000000, -0.000000000000000000, -0.000000000000000000 ) ) ;
#1936=DIRECTION ( 'NONE',  ( -1.000000000000000000, -0.000000000000000000, -0.000000000000000000 ) ) ;
#1938=AXIS2_PLACEMENT_3D ( 'NONE', #3176, #2573, #1020 ) ;
#1946=VECTOR ( 'NONE', #1483, 1000.000000000000000 ) ;
#1958=UNCERTAINTY_MEASURE_WITH_UNIT (LENGTH_MEASURE( 1.000000000000000082E-05 ), #3266, 'distance_accuracy_value', 'NONE');
#1961=DIRECTION ( 'NONE',  ( 0.000000000000000000, 0.000000000000000000, 1.000000000000000000 ) ) ;
#1963=AXIS2_PLACEMENT_3D ( 'NONE', #3021, #1510, #2708 ) ;
#1968=CARTESIAN_POINT ( 'NONE',  ( 8.673617379884035472E-16, 0.000000000000000000, 0.000000000000000000 ) ) ;
#1978=EDGE_LOOP ( 'NONE', ( #3148, #2950, #2603 ) ) ;
#1987=UNCERTAINTY_MEASURE_WITH_UNIT (LENGTH_MEASURE( 1.000000000000000082E-05 ), #3301, 'distance_accuracy_value', 'NONE');
#1989=DIRECTION ( 'NONE',  ( -1.000000000000000000, -0.000000000000000000, -0.000000000000000000 ) ) ;
#1995=MANIFOLD_SOLID_BREP ( 'Hex', #2346 ) ;
#2004=VECTOR ( 'NONE', #3364, 1000.000000000000000 ) ;
#2010=AXIS2_PLACEMENT_3D ( 'NONE', #3818, #1156, #2344 ) ;
#2019=EDGE_CURVE ( 'NONE', #3147, #1255, #1263, .T. ) ;
#2020=CIRCLE ( 'NONE', #2515, 1.250000000000000222 ) ;
#2022=VECTOR ( 'NONE', #1538, 1000.000000000000000 ) ;
#2028=CIRCLE ( 'NONE', #150, 3.799999999999999378 ) ;
#2029=CIRCLE ( 'NONE', #334, 3.799999999999999378 ) ;
#2032=CARTESIAN_POINT ( 'NONE',  ( 1.300000000000000044, 0.000000000000000000, -1.250000000000000000 ) ) ;
#2033=EDGE_CURVE ( 'NONE', #1187, #1528, #2394, .T. ) ;
#2034=PRODUCT_DEFINITION_FORMATION_WITH_SPECIFIED_SOURCE ( 'ANY', '', #1795, .NOT_KNOWN. ) ;
#2036=VERTEX_POINT ( 'NONE', #57 ) ;
#2045=ORIENTED_EDGE ( 'NONE', *, *, #684, .T. ) ;
#2046=DIRECTION ( 'NONE',  ( -0.000000000000000000, -0.5000000000000001110, 0.8660254037844385966 ) ) ;
#2049=DIRECTION ( 'NONE',  ( -0.000000000000000000, 1.000000000000000000, -0.000000000000000000 ) ) ;
#2057=DIRECTION ( 'NONE',  ( 1.000000000000000000, 0.000000000000000000, 0.000000000000000000 ) ) ;
#2066=DIRECTION ( 'NONE',  ( -1.000000000000000000, -0.000000000000000000, -0.000000000000000000 ) ) ;
#2068=VECTOR ( 'NONE', #44, 1000.000000000000114 ) ;
#2070=EDGE_CURVE ( 'NONE', #1408, #1, #1139, .T. ) ;
#2076=EDGE_LOOP ( 'NONE', ( #2425, #3757, #3548, #946 ) ) ;
#2080=FACE_OUTER_BOUND ( 'NONE', #949, .T. ) ;
#2089=( GEOMETRIC_REPRESENTATION_CONTEXT ( 3 ) GLOBAL_UNCERTAINTY_ASSIGNED_CONTEXT ( ( #3128 ) ) GLOBAL_UNIT_ASSIGNED_CONTEXT ( ( #3795, #3834, #898 ) ) REPRESENTATION_CONTEXT ( 'NONE', 'WORKASPACE' ) );
#2092=VERTEX_POINT ( 'NONE', #3122 ) ;
#2105=CARTESIAN_POINT ( 'NONE',  ( 1.300000000000000044, -0.7216878364870317197, -1.250000000000000000 ) ) ;
#2109=ORIENTED_EDGE ( 'NONE', *, *, #1410, .T. ) ;
#2112=ORIENTED_EDGE ( 'NONE', *, *, #808, .F. ) ;
#2114=ORIENTED_EDGE ( 'NONE', *, *, #1698, .F. ) ;
#2115=CARTESIAN_POINT ( 'NONE',  ( 2.021687836487040535, 2.655529440325959183E-32, -2.168404344971008868E-16 ) ) ;
#2118=CARTESIAN_POINT ( 'NONE',  ( 1.300000000000000044, 1.443375672974065216, 7.222237291452134449E-31 ) ) ;
#2119=FACE_OUTER_BOUND ( 'NONE', #3469, .T. ) ;
#2120=LINE ( 'NONE', #2453, #219 ) ;
#2122=ORIENTED_EDGE ( 'NONE', *, *, #719, .F. ) ;
#2131=CIRCLE ( 'NONE', #2010, 3.799999999999999378 ) ;
#2133=ORIENTED_EDGE ( 'NONE', *, *, #507, .T. ) ;
#2139=CARTESIAN_POINT ( 'NONE',  ( 1.300000000000000044, -0.7216878364870317197, 1.250000000000000000 ) ) ;
#2146=AXIS2_PLACEMENT_3D ( 'NONE', #3805, #224, #2616 ) ;
#2147=ORIENTED_EDGE ( 'NONE', *, *, #3609, .T. ) ;
#2153=EDGE_CURVE ( 'NONE', #137, #511, #1650, .T. ) ;
#2157=LINE ( 'NONE', #738, #1771 ) ;
#2158=( NAMED_UNIT ( * ) SI_UNIT ( $, .STERADIAN. ) SOLID_ANGLE_UNIT ( ) );
#2170=VERTEX_POINT ( 'NONE', #2502 ) ;
#2172=LINE ( 'NONE', #3360, #3575 ) ;
#2182=EDGE_CURVE ( 'NONE', #1255, #2698, #1057, .T. ) ;
#2187=CARTESIAN_POINT ( 'NONE',  ( 3.885274725274725949, -4.336808689942017736E-16, 0.000000000000000000 ) ) ;
#2191=DIRECTION ( 'NONE',  ( 0.000000000000000000, 0.5000000000000002220, 0.8660254037844384856 ) ) ;
#2197=CARTESIAN_POINT ( 'NONE',  ( 11.80999999999999872, 0.000000000000000000, 0.000000000000000000 ) ) ;
#2199=CONICAL_SURFACE ( 'NONE', #3566, 1732.050807568857181, 1.047197551196592746 ) ;
#2207=AXIS2_PLACEMENT_3D ( 'NONE', #820, #2246, #3194 ) ;
#2210=CIRCLE ( 'NONE', #532, 1.250000000000000222 ) ;
#2224=DIRECTION ( 'NONE',  ( 0.000000000000000000, -0.5000000000000002220, 0.8660254037844384856 ) ) ;
#2232=ADVANCED_FACE ( 'NONE', ( #3491 ), #3806, .T. ) ;
#2235=DIRECTION ( 'NONE',  ( -1.000000000000000000, -0.000000000000000000, -0.000000000000000000 ) ) ;
#2236=PLANE ( 'NONE',  #3461 ) ;
#2240=LINE ( 'NONE', #2485, #1648 ) ;
#2245=CARTESIAN_POINT ( 'NONE',  ( 1.300000000000000044, 1.443375672974065216, 7.222237291452134449E-31 ) ) ;
#2246=DIRECTION ( 'NONE',  ( 0.000000000000000000, 0.000000000000000000, 1.000000000000000000 ) ) ;
#2248=LINE ( 'NONE', #2596, #2627 ) ;
#2250=FACE_OUTER_BOUND ( 'NONE', #3080, .T. ) ;
#2255=CYLINDRICAL_SURFACE ( 'NONE', #1032, 3.799999999999999378 ) ;
#2256=DIRECTION ( 'NONE',  ( -1.000000000000000000, 0.000000000000000000, 0.000000000000000000 ) ) ;
#2257=AXIS2_PLACEMENT_3D ( 'NONE', #1635, #2824, #1062 ) ;
#2260=DIRECTION ( 'NONE',  ( -1.000000000000000000, -0.000000000000000000, -0.000000000000000000 ) ) ;
#2264=AXIS2_PLACEMENT_3D ( 'NONE', #3223, #2057, #814 ) ;
#2267=DIRECTION ( 'NONE',  ( 0.000000000000000000, -0.8660254037844387076, 0.5000000000000001110 ) ) ;
#2273=DIRECTION ( 'NONE',  ( -1.000000000000000000, -0.000000000000000000, -0.000000000000000000 ) ) ;
#2278=EDGE_LOOP ( 'NONE', ( #3775, #807, #552 ) ) ;
#2285=CIRCLE ( 'NONE', #3209, 1.250000000000000222 ) ;
#2292=EDGE_CURVE ( 'NONE', #2698, #3067, #1757, .T. ) ;
#2306=CARTESIAN_POINT ( 'NONE',  ( 2.399999999999999911, 2.694222958124176020E-16, -2.199999999999999289 ) ) ;
#2311=EDGE_CURVE ( 'NONE', #3430, #964, #2602, .T. ) ;
#2316=ORIENTED_EDGE ( 'NONE', *, *, #2033, .F. ) ;
#2317=DIRECTION ( 'NONE',  ( 0.000000000000000000, 0.000000000000000000, 1.000000000000000000 ) ) ;
#2322=EDGE_LOOP ( 'NONE', ( #1504, #3204, #113, #3726, #2540 ) ) ;
#2330=CIRCLE ( 'NONE', #1086, 2.199999999999999289 ) ;
#2336=ORIENTED_EDGE ( 'NONE', *, *, #3609, .F. ) ;
#2339=CIRCLE ( 'NONE', #463, 4.324969328314201000 ) ;
#2340=ORIENTED_EDGE ( 'NONE', *, *, #804, .T. ) ;
#2342=FACE_OUTER_BOUND ( 'NONE', #1978, .T. ) ;
#2344=DIRECTION ( 'NONE',  ( 0.000000000000000000, 0.000000000000000000, 1.000000000000000000 ) ) ;
#2346=CLOSED_SHELL ( 'NONE', ( #1846, #3208, #492, #2680, #555, #2906, #1605, #2865, #1252, #439, #2755, #608, #3146, #2514, #431, #1360, #1535, #1304, #3672, #2232, #1488, #1422, #2510, #1290, #2641, #2712, #2665 ) ) ;
#2347=ORIENTED_EDGE ( 'NONE', *, *, #3730, .T. ) ;
#2356=CARTESIAN_POINT ( 'NONE',  ( 2.399999999999999911, 0.000000000000000000, 0.000000000000000000 ) ) ;
#2365=VERTEX_POINT ( 'NONE', #2720 ) ;
#2366=DIRECTION ( 'NONE',  ( -0.000000000000000000, -0.5000000000000002220, -0.8660254037844384856 ) ) ;
#2368=CARTESIAN_POINT ( 'NONE',  ( 8.673617379884035472E-16, 1.899999999999999689, 0.000000000000000000 ) ) ;
#2370=DIRECTION ( 'NONE',  ( 0.000000000000000000, 0.000000000000000000, 1.000000000000000000 ) ) ;
#2378=CONICAL_SURFACE ( 'NONE', #2435, 1732.050807568857181, 1.047197551196592746 ) ;
#2379=EDGE_CURVE ( 'NONE', #2443, #1873, #3134, .T. ) ;
#2388=EDGE_CURVE ( 'NONE', #1346, #620, #1545, .T. ) ;
#2390=VECTOR ( 'NONE', #3234, 1000.000000000000000 ) ;
#2394=LINE ( 'NONE', #1531, #1019 ) ;
#2402=AXIS2_PLACEMENT_3D ( 'NONE', #2732, #60, #2431 ) ;
#2403=DIRECTION ( 'NONE',  ( -1.000000000000000000, -0.000000000000000000, -0.000000000000000000 ) ) ;
#2405=VECTOR ( 'NONE', #2046, 1000.000000000000000 ) ;
#2413=( NAMED_UNIT ( * ) PLANE_ANGLE_UNIT ( ) SI_UNIT ( $, .RADIAN. ) );
#2421=DIRECTION ( 'NONE',  ( 0.000000000000000000, 0.000000000000000000, 1.000000000000000000 ) ) ;
#2425=ORIENTED_EDGE ( 'NONE', *, *, #49, .T. ) ;
#2429=DIRECTION ( 'NONE',  ( -0.5000000000000042188, 0.000000000000000000, 0.8660254037844361541 ) ) ;
#2431=DIRECTION ( 'NONE',  ( -0.000000000000000000, 0.000000000000000000, -1.000000000000000000 ) ) ;
#2432=CARTESIAN_POINT ( 'NONE',  ( 1.300000000000000044, 0.7216878364870329410, 1.249999999999999778 ) ) ;
#2435=AXIS2_PLACEMENT_3D ( 'NONE', #3697, #109, #1303 ) ;
#2443=VERTEX_POINT ( 'NONE', #2368 ) ;
#2451=AXIS2_PLACEMENT_3D ( 'NONE', #2306, #745, #2825 ) ;
#2453=CARTESIAN_POINT ( 'NONE',  ( 0.000000000000000000, 0.000000000000000000, 3.799999999999999378 ) ) ;
#2456=ORIENTED_EDGE ( 'NONE', *, *, #1254, .F. ) ;
#2475=ORIENTED_EDGE ( 'NONE', *, *, #612, .F. ) ;
#2477=ORIENTED_EDGE ( 'NONE', *, *, #49, .F. ) ;
#2479=DIRECTION ( 'NONE',  ( 0.000000000000000000, 1.000000000000000000, 0.000000000000000000 ) ) ;
#2485=CARTESIAN_POINT ( 'NONE',  ( 1.300000000000000044, 0.7216878364870329410, 1.249999999999999778 ) ) ;
#2496=CIRCLE ( 'NONE', #1938, 1.250000000000000222 ) ;
#2501=CARTESIAN_POINT ( 'NONE',  ( 2.199999999999999734, 1.999999999999999112, 0.000000000000000000 ) ) ;
#2502=CARTESIAN_POINT ( 'NONE',  ( 1.820000000000000062, 4.653657836759941744E-16, -3.799999999999999378 ) ) ;
#2503=VECTOR ( 'NONE', #568, 1000.000000000000227 ) ;
#2505=DIRECTION ( 'NONE',  ( -1.000000000000000000, -0.000000000000000000, -0.000000000000000000 ) ) ;
#2510=ADVANCED_FACE ( 'NONE', ( #614 ), #1800, .F. ) ;
#2512=FACE_OUTER_BOUND ( 'NONE', #3037, .T. ) ;
#2514=ADVANCED_FACE ( 'NONE', ( #631 ), #324, .F. ) ;
#2515=AXIS2_PLACEMENT_3D ( 'NONE', #2838, #455, #290 ) ;
#2529=DIRECTION ( 'NONE',  ( -1.000000000000000000, 0.000000000000000000, -0.000000000000000000 ) ) ;
#2537=CARTESIAN_POINT ( 'NONE',  ( 1.300000000000000044, -0.7216878364870317197, -1.250000000000000000 ) ) ;
#2540=ORIENTED_EDGE ( 'NONE', *, *, #2153, .F. ) ;
#2545=DIRECTION ( 'NONE',  ( 0.000000000000000000, 0.000000000000000000, -1.000000000000000000 ) ) ;
#2546=ORIENTED_EDGE ( 'NONE', *, *, #3332, .T. ) ;
#2548=DIRECTION ( 'NONE',  ( -1.000000000000000000, -0.000000000000000000, -0.000000000000000000 ) ) ;
#2550=EDGE_LOOP ( 'NONE', ( #216, #1208, #3495 ) ) ;
#2554=PLANE ( 'NONE',  #1719 ) ;
#2556=VERTEX_POINT ( 'NONE', #3648 ) ;
#2559=FACE_OUTER_BOUND ( 'NONE', #2867, .T. ) ;
#2573=DIRECTION ( 'NONE',  ( -1.000000000000000000, -0.000000000000000000, -0.000000000000000000 ) ) ;
#2596=CARTESIAN_POINT ( 'NONE',  ( 0.000000000000000000, -1.443375672974064328, 1.278502688459867223E-18 ) ) ;
#2601=LINE ( 'NONE', #1688, #3027 ) ;
#2602=LINE ( 'NONE', #1414, #1324 ) ;
#2603=ORIENTED_EDGE ( 'NONE', *, *, #1575, .F. ) ;
#2614=EDGE_LOOP ( 'NONE', ( #3819, #384 ) ) ;
#2616=DIRECTION ( 'NONE',  ( 0.000000000000000000, 0.000000000000000000, -1.000000000000000000 ) ) ;
#2618=EDGE_CURVE ( 'NONE', #2365, #2875, #2330, .T. ) ;
#2620=CARTESIAN_POINT ( 'NONE',  ( 1.300000000000000044, 0.7216878364870329410, -1.250000000000000000 ) ) ;
#2626=CARTESIAN_POINT ( 'NONE',  ( 1.300000000000000044, 0.7216878364870329410, -1.250000000000000000 ) ) ;
#2627=VECTOR ( 'NONE', #234, 1000.000000000000114 ) ;
#2633=VERTEX_POINT ( 'NONE', #98 ) ;
#2634=EDGE_CURVE ( 'NONE', #691, #2633, #3375, .T. ) ;
#2638=CARTESIAN_POINT ( 'NONE',  ( 12.20000000000000107, 0.000000000000000000, 0.000000000000000000 ) ) ;
#2641=ADVANCED_FACE ( 'NONE', ( #2250 ), #1294, .F. ) ;
#2650=CIRCLE ( 'NONE', #2146, 0.2000000000000000944 ) ;
#2654=DIRECTION ( 'NONE',  ( 1.000000000000000000, 0.000000000000000000, -0.000000000000000000 ) ) ;
#2665=ADVANCED_FACE ( 'NONE', ( #2559 ), #2199, .F. ) ;
#2678=LINE ( 'NONE', #2718, #587 ) ;
#2680=ADVANCED_FACE ( 'NONE', ( #2080 ), #634, .T. ) ;
#2683=DIRECTION ( 'NONE',  ( 0.000000000000000000, 0.000000000000000000, 1.000000000000000000 ) ) ;
#2689=DIRECTION ( 'NONE',  ( -0.000000000000000000, 0.000000000000000000, 1.000000000000000000 ) ) ;
#2694=VECTOR ( 'NONE', #2786, 1000.000000000000000 ) ;
#2698=VERTEX_POINT ( 'NONE', #1802 ) ;
#2703=DIRECTION ( 'NONE',  ( -0.000000000000000000, 0.000000000000000000, -1.000000000000000000 ) ) ;
#2708=DIRECTION ( 'NONE',  ( 0.000000000000000000, 0.000000000000000000, 1.000000000000000000 ) ) ;
#2709=FACE_BOUND ( 'NONE', #932, .T. ) ;
#2712=ADVANCED_FACE ( 'NONE', ( #1505 ), #1825, .F. ) ;
#2715=ORIENTED_EDGE ( 'NONE', *, *, #667, .F. ) ;
#2718=CARTESIAN_POINT ( 'NONE',  ( 1.300000000000000044, -1.443375672974064328, 1.278502688459867223E-18 ) ) ;
#2720=CARTESIAN_POINT ( 'NONE',  ( 2.199999999999999734, 2.694222958124176020E-16, -2.199999999999999289 ) ) ;
#2724=DIRECTION ( 'NONE',  ( -1.000000000000000000, -0.000000000000000000, -0.000000000000000000 ) ) ;
#2726=DIRECTION ( 'NONE',  ( -0.000000000000000000, -0.5000000000000002220, -0.8660254037844384856 ) ) ;
#2729=PLANE ( 'NONE',  #1559 ) ;
#2732=CARTESIAN_POINT ( 'NONE',  ( 1.300000000000000044, -1.443375672974064328, 2.168404344971008868E-16 ) ) ;
#2737=CARTESIAN_POINT ( 'NONE',  ( 1.300000000000000044, 0.7216878364870329410, 1.249999999999999778 ) ) ;
#2738=EDGE_CURVE ( 'NONE', #1516, #1495, #602, .T. ) ;
#2742=CARTESIAN_POINT ( 'NONE',  ( 1.300000000000000044, -1.443375672974064328, 1.278502688459867223E-18 ) ) ;
#2752=CARTESIAN_POINT ( 'NONE',  ( 2.199999999999999734, 0.000000000000000000, 0.000000000000000000 ) ) ;
#2755=ADVANCED_FACE ( 'NONE', ( #3616 ), #3038, .T. ) ;
#2767=CIRCLE ( 'NONE', #1775, 2.199999999999999289 ) ;
#2768=DIRECTION ( 'NONE',  ( 0.000000000000000000, 0.000000000000000000, 1.000000000000000000 ) ) ;
#2773=CONICAL_SURFACE ( 'NONE', #1888, 1.610000000000000098, 0.7853981633974458365 ) ;
#2776=ORIENTED_EDGE ( 'NONE', *, *, #3332, .F. ) ;
#2786=DIRECTION ( 'NONE',  ( -0.000000000000000000, -0.5000000000000001110, 0.8660254037844385966 ) ) ;
#2810=DIRECTION ( 'NONE',  ( 0.000000000000000000, 1.000000000000000000, 0.000000000000000000 ) ) ;
#2814=DIRECTION ( 'NONE',  ( -0.000000000000000000, -1.000000000000000000, 1.502314598737159031E-16 ) ) ;
#2824=DIRECTION ( 'NONE',  ( 1.000000000000000000, 0.000000000000000000, -0.000000000000000000 ) ) ;
#2825=DIRECTION ( 'NONE',  ( 0.000000000000000000, -1.224646799147353207E-16, 1.000000000000000000 ) ) ;
#2838=CARTESIAN_POINT ( 'NONE',  ( 1.300000000000000044, 0.000000000000000000, 0.000000000000000000 ) ) ;
#2843=CARTESIAN_POINT ( 'NONE',  ( 0.000000000000000000, 1.443375672974065216, 7.222237291452134449E-31 ) ) ;
#2856=DIRECTION ( 'NONE',  ( -1.000000000000000000, -0.000000000000000000, -0.000000000000000000 ) ) ;
#2857=DIRECTION ( 'NONE',  ( 0.000000000000000000, 0.000000000000000000, 1.000000000000000000 ) ) ;
#2860=DIRECTION ( 'NONE',  ( -1.000000000000000000, -0.000000000000000000, -0.000000000000000000 ) ) ;
#2865=ADVANCED_FACE ( 'NONE', ( #3551 ), #426, .T. ) ;
#2867=EDGE_LOOP ( 'NONE', ( #1426, #2045, #543, #1867, #3313 ) ) ;
#2868=DIRECTION ( 'NONE',  ( -1.000000000000000000, 0.000000000000000000, 0.000000000000000000 ) ) ;
#2870=ADVANCED_BREP_SHAPE_REPRESENTATION ( '', ( #1995, #2207 ), #1040 ) ;
#2875=VERTEX_POINT ( 'NONE', #1296 ) ;
#2881=AXIS2_PLACEMENT_3D ( 'NONE', #2187, #3712, #2810 ) ;
#2882=CARTESIAN_POINT ( 'NONE',  ( 1.300000000000000044, 1.082531754730549300, 0.6250000000000008882 ) ) ;
#2884=AXIS2_PLACEMENT_3D ( 'NONE', #2638, #1465, #1498 ) ;
#2886=DIRECTION ( 'NONE',  ( -0.000000000000000000, 1.000000000000000000, -0.000000000000000000 ) ) ;
#2906=ADVANCED_FACE ( 'NONE', ( #1006 ), #1620, .T. ) ;
#2929=ORIENTED_EDGE ( 'NONE', *, *, #719, .T. ) ;
#2935=DIRECTION ( 'NONE',  ( -1.000000000000000000, -0.000000000000000000, -0.000000000000000000 ) ) ;
#2938=VECTOR ( 'NONE', #19, 1000.000000000000000 ) ;
#2942=PLANE ( 'NONE',  #3124 ) ;
#2950=ORIENTED_EDGE ( 'NONE', *, *, #3613, .F. ) ;
#2968=CARTESIAN_POINT ( 'NONE',  ( 1.300000000000000044, 0.7216878364870329410, -1.250000000000000000 ) ) ;
#2977=EDGE_LOOP ( 'NONE', ( #1555, #778, #711, #3550 ) ) ;
#2981=SURFACE_STYLE_FILL_AREA ( #3228 ) ;
#2983=DIRECTION ( 'NONE',  ( -0.000000000000000000, 0.5000000000000000000, 0.8660254037844385966 ) ) ;
#2990=FACE_OUTER_BOUND ( 'NONE', #766, .T. ) ;
#2992=DIRECTION ( 'NONE',  ( 1.000000000000000000, 0.000000000000000000, -0.000000000000000000 ) ) ;
#3000=DIRECTION ( 'NONE',  ( -0.000000000000000000, 1.000000000000000000, -0.000000000000000000 ) ) ;
#3009=EDGE_LOOP ( 'NONE', ( #1787, #1424, #3478, #2147, #3748 ) ) ;
#3021=CARTESIAN_POINT ( 'NONE',  ( 12.20000000000000107, 0.000000000000000000, 0.000000000000000000 ) ) ;
#3027=VECTOR ( 'NONE', #2868, 1000.000000000000000 ) ;
#3028=PLANE ( 'NONE',  #2402 ) ;
#3030=LINE ( 'NONE', #1613, #2022 ) ;
#3033=FACE_OUTER_BOUND ( 'NONE', #2977, .T. ) ;
#3037=EDGE_LOOP ( 'NONE', ( #226, #2112, #2715 ) ) ;
#3038=CYLINDRICAL_SURFACE ( 'NONE', #1570, 1.999999999999999112 ) ;
#3060=DIRECTION ( 'NONE',  ( -0.000000000000000000, -1.000000000000000000, 1.502314598737159031E-16 ) ) ;
#3064=AXIS2_PLACEMENT_3D ( 'NONE', #762, #440, #3723 ) ;
#3067=VERTEX_POINT ( 'NONE', #1739 ) ;
#3073=EDGE_LOOP ( 'NONE', ( #3814, #3544, #524, #366, #67 ) ) ;
#3079=DIRECTION ( 'NONE',  ( -0.000000000000000000, -0.5000000000000001110, 0.8660254037844385966 ) ) ;
#3080=EDGE_LOOP ( 'NONE', ( #2336, #1474, #2316 ) ) ;
#3081=DIRECTION ( 'NONE',  ( -0.000000000000000000, 0.5000000000000000000, 0.8660254037844385966 ) ) ;
#3085=DIRECTION ( 'NONE',  ( -1.000000000000000000, -0.000000000000000000, -0.000000000000000000 ) ) ;
#3093=CARTESIAN_POINT ( 'NONE',  ( 1.300000000000000044, -1.443375672974064328, 2.168404344971008868E-16 ) ) ;
#3101=APPLICATION_CONTEXT ( 'automotive_design' ) ;
#3102=CARTESIAN_POINT ( 'NONE',  ( 3.885274725274725949, -4.336808689942017736E-16, 0.000000000000000000 ) ) ;
#3108=DIRECTION ( 'NONE',  ( 0.000000000000000000, 0.000000000000000000, 1.000000000000000000 ) ) ;
#3122=CARTESIAN_POINT ( 'NONE',  ( 1.820000000000000062, -3.799999999999999378, -4.653657836759940757E-16 ) ) ;
#3124=AXIS2_PLACEMENT_3D ( 'NONE', #3272, #2654, #1171 ) ;
#3126=EDGE_LOOP ( 'NONE', ( #2347, #1914, #2109, #1064, #1616 ) ) ;
#3128=UNCERTAINTY_MEASURE_WITH_UNIT (LENGTH_MEASURE( 1.000000000000000082E-05 ), #3795, 'distance_accuracy_value', 'NONE');
#3133=DIRECTION ( 'NONE',  ( 0.000000000000000000, 0.000000000000000000, 1.000000000000000000 ) ) ;
#3134=CIRCLE ( 'NONE', #3625, 1.899999999999999689 ) ;
#3136=EDGE_CURVE ( 'NONE', #1729, #1187, #2678, .T. ) ;
#3146=ADVANCED_FACE ( 'NONE', ( #2990 ), #308, .F. ) ;
#3147=VERTEX_POINT ( 'NONE', #889 ) ;
#3148=ORIENTED_EDGE ( 'NONE', *, *, #1327, .F. ) ;
#3149=CARTESIAN_POINT ( 'NONE',  ( -997.9783121635130101, 0.000000000000000000, 0.000000000000000000 ) ) ;
#3153=ORIENTED_EDGE ( 'NONE', *, *, #802, .T. ) ;
#3160=CARTESIAN_POINT ( 'NONE',  ( 1.300000000000000044, 0.000000000000000000, 0.000000000000000000 ) ) ;
#3166=EDGE_CURVE ( 'NONE', #1346, #929, #12, .T. ) ;
#3176=CARTESIAN_POINT ( 'NONE',  ( 1.300000000000000044, 0.000000000000000000, 0.000000000000000000 ) ) ;
#3178=ORIENTED_EDGE ( 'NONE', *, *, #549, .F. ) ;
#3182=CARTESIAN_POINT ( 'NONE',  ( 1.300000000000000044, 0.000000000000000000, 0.000000000000000000 ) ) ;
#3190=CIRCLE ( 'NONE', #643, 1.610000000000000098 ) ;
#3191=AXIS2_PLACEMENT_3D ( 'NONE', #3442, #1624, #2857 ) ;
#3194=DIRECTION ( 'NONE',  ( 1.000000000000000000, 0.000000000000000000, 0.000000000000000000 ) ) ;
#3200=AXIS2_PLACEMENT_3D ( 'NONE', #169, #1936, #3133 ) ;
#3204=ORIENTED_EDGE ( 'NONE', *, *, #667, .T. ) ;
#3208=ADVANCED_FACE ( 'NONE', ( #3033 ), #1707, .F. ) ;
#3209=AXIS2_PLACEMENT_3D ( 'NONE', #3182, #2856, #1961 ) ;
#3210=VERTEX_POINT ( 'NONE', #1481 ) ;
#3214=EDGE_LOOP ( 'NONE', ( #3732, #281, #1479 ) ) ;
#3218=ORIENTED_EDGE ( 'NONE', *, *, #2618, .T. ) ;
#3223=CARTESIAN_POINT ( 'NONE',  ( 2.399999999999999911, 0.000000000000000000, 0.000000000000000000 ) ) ;
#3228=FILL_AREA_STYLE ('',( #1677 ) ) ;
#3231=CARTESIAN_POINT ( 'NONE',  ( 1.300000000000000044, 1.443375672974065216, 7.222237291452134449E-31 ) ) ;
#3232=ORIENTED_EDGE ( 'NONE', *, *, #604, .F. ) ;
#3234=DIRECTION ( 'NONE',  ( -0.000000000000000000, -1.000000000000000000, 1.502314598737159031E-16 ) ) ;
#3248=CARTESIAN_POINT ( 'NONE',  ( 2.021687836487040535, 0.000000000000000000, 2.168404344971008868E-16 ) ) ;
#3263=ORIENTED_EDGE ( 'NONE', *, *, #134, .F. ) ;
#3266=( LENGTH_UNIT ( ) NAMED_UNIT ( * ) SI_UNIT ( .MILLI., .METRE. ) );
#3269=LINE ( 'NONE', #2118, #1717 ) ;
#3272=CARTESIAN_POINT ( 'NONE',  ( 1.300000000000000044, -1.443375672974064328, 2.168404344971008868E-16 ) ) ;
#3283=ORIENTED_EDGE ( 'NONE', *, *, #3606, .F. ) ;
#3295=ORIENTED_EDGE ( 'NONE', *, *, #1626, .T. ) ;
#3301=( LENGTH_UNIT ( ) NAMED_UNIT ( * ) SI_UNIT ( .MILLI., .METRE. ) );
#3302=EDGE_CURVE ( 'NONE', #2633, #1495, #1853, .T. ) ;
#3305=DIRECTION ( 'NONE',  ( -1.000000000000000000, 0.000000000000000000, -0.000000000000000000 ) ) ;
#3313=ORIENTED_EDGE ( 'NONE', *, *, #1327, .T. ) ;
#3332=EDGE_CURVE ( 'NONE', #2556, #3430, #2248, .T. ) ;
#3338=ORIENTED_EDGE ( 'NONE', *, *, #196, .F. ) ;
#3347=CARTESIAN_POINT ( 'NONE',  ( 12.20000000000000107, 1.971681346627238735E-16, -1.610000000000000098 ) ) ;
#3349=CARTESIAN_POINT ( 'NONE',  ( 1.300000000000000044, -0.7216878364870317197, 1.250000000000000000 ) ) ;
#3360=CARTESIAN_POINT ( 'NONE',  ( 0.000000000000000000, 4.653657836759941744E-16, -3.799999999999999378 ) ) ;
#3364=DIRECTION ( 'NONE',  ( -1.000000000000000000, 0.000000000000000000, 0.000000000000000000 ) ) ;
#3366=PRODUCT_DEFINITION ( 'UNKNOWN', '', #2034, #1685 ) ;
#3374=ORIENTED_EDGE ( 'NONE', *, *, #1092, .T. ) ;
#3375=LINE ( 'NONE', #3414, #25 ) ;
#3382=FACE_BOUND ( 'NONE', #246, .T. ) ;
#3393=EDGE_LOOP ( 'NONE', ( #888, #1191, #1601, #3338, #944 ) ) ;
#3403=FACE_OUTER_BOUND ( 'NONE', #2076, .T. ) ;
#3405=DIRECTION ( 'NONE',  ( -1.000000000000000000, 0.000000000000000000, 0.000000000000000000 ) ) ;
#3414=CARTESIAN_POINT ( 'NONE',  ( 1.300000000000000044, -0.7216878364870317197, -1.250000000000000000 ) ) ;
#3423=CARTESIAN_POINT ( 'NONE',  ( 12.20000000000000107, 0.000000000000000000, 0.000000000000000000 ) ) ;
#3428=DIRECTION ( 'NONE',  ( 0.000000000000000000, 0.8660254037844385966, 0.5000000000000003331 ) ) ;
#3430=VERTEX_POINT ( 'NONE', #1665 ) ;
#3442=CARTESIAN_POINT ( 'NONE',  ( 1.300000000000000044, 0.000000000000000000, 0.000000000000000000 ) ) ;
#3461=AXIS2_PLACEMENT_3D ( 'NONE', #2742, #146, #2191 ) ;
#3469=EDGE_LOOP ( 'NONE', ( #3502, #896 ) ) ;
#3478=ORIENTED_EDGE ( 'NONE', *, *, #1051, .T. ) ;
#3487=AXIS2_PLACEMENT_3D ( 'NONE', #2968, #904, #607 ) ;
#3491=FACE_OUTER_BOUND ( 'NONE', #529, .T. ) ;
#3495=ORIENTED_EDGE ( 'NONE', *, *, #3705, .F. ) ;
#3498=SHAPE_REPRESENTATION_RELATIONSHIP ( 'NONE' , 'NONE' ,  #556, #2870 ) ;
#3502=ORIENTED_EDGE ( 'NONE', *, *, #2379, .T. ) ;
#3503=AXIS2_PLACEMENT_3D ( 'NONE', #1183, #1225, #2683 ) ;
#3526=CARTESIAN_POINT ( 'NONE',  ( 1.300000000000000044, 0.000000000000000000, 0.000000000000000000 ) ) ;
#3528=ORIENTED_EDGE ( 'NONE', *, *, #604, .T. ) ;
#3541=LINE ( 'NONE', #1420, #632 ) ;
#3544=ORIENTED_EDGE ( 'NONE', *, *, #549, .T. ) ;
#3548=ORIENTED_EDGE ( 'NONE', *, *, #1776, .F. ) ;
#3550=ORIENTED_EDGE ( 'NONE', *, *, #1092, .F. ) ;
#3551=FACE_OUTER_BOUND ( 'NONE', #31, .T. ) ;
#3555=SURFACE_SIDE_STYLE ('',( #2981 ) ) ;
#3563=VECTOR ( 'NONE', #1673, 1000.000000000000000 ) ;
#3566=AXIS2_PLACEMENT_3D ( 'NONE', #3149, #2273, #1668 ) ;
#3571=ORIENTED_EDGE ( 'NONE', *, *, #835, .T. ) ;
#3575=VECTOR ( 'NONE', #1876, 1000.000000000000000 ) ;
#3581=DIRECTION ( 'NONE',  ( 0.000000000000000000, 0.000000000000000000, 1.000000000000000000 ) ) ;
#3589=DIRECTION ( 'NONE',  ( -1.000000000000000000, -0.000000000000000000, -0.000000000000000000 ) ) ;
#3592=ORIENTED_EDGE ( 'NONE', *, *, #2311, .T. ) ;
#3600=EDGE_CURVE ( 'NONE', #1136, #1813, #2131, .T. ) ;
#3603=FACE_OUTER_BOUND ( 'NONE', #2278, .T. ) ;
#3605=EDGE_LOOP ( 'NONE', ( #3295, #1629, #2929, #1366, #1816 ) ) ;
#3606=EDGE_CURVE ( 'NONE', #3147, #3210, #3190, .T. ) ;
#3609=EDGE_CURVE ( 'NONE', #691, #1187, #139, .T. ) ;
#3611=DIRECTION ( 'NONE',  ( 0.000000000000000000, 0.000000000000000000, 1.000000000000000000 ) ) ;
#3613=EDGE_CURVE ( 'NONE', #137, #1, #872, .T. ) ;
#3616=FACE_OUTER_BOUND ( 'NONE', #1464, .T. ) ;
#3625=AXIS2_PLACEMENT_3D ( 'NONE', #931, #354, #3611 ) ;
#3640=CIRCLE ( 'NONE', #3828, 1.899999999999999689 ) ;
#3642=FACE_OUTER_BOUND ( 'NONE', #3393, .T. ) ;
#3648=CARTESIAN_POINT ( 'NONE',  ( 4.336808689942017736E-16, -0.7216878364870317197, 1.250000000000000000 ) ) ;
#3655=CARTESIAN_POINT ( 'NONE',  ( 2.200000000000000178, 0.000000000000000000, 0.000000000000000000 ) ) ;
#3672=ADVANCED_FACE ( 'NONE', ( #3642 ), #112, .T. ) ;
#3676=CARTESIAN_POINT ( 'NONE',  ( 1.820000000000000062, 0.000000000000000000, 0.000000000000000000 ) ) ;
#3683=ORIENTED_EDGE ( 'NONE', *, *, #1525, .T. ) ;
#3685=AXIS2_PLACEMENT_3D ( 'NONE', #3526, #3589, #925 ) ;
#3690=DIRECTION ( 'NONE',  ( 0.000000000000000000, 0.000000000000000000, 1.000000000000000000 ) ) ;
#3691=PLANE ( 'NONE',  #1590 ) ;
#3695=DIRECTION ( 'NONE',  ( 1.000000000000000000, 0.000000000000000000, 0.000000000000000000 ) ) ;
#3697=CARTESIAN_POINT ( 'NONE',  ( -997.9783121635130101, 0.000000000000000000, 0.000000000000000000 ) ) ;
#3698=VECTOR ( 'NONE', #3000, 1000.000000000000000 ) ;
#3703=DIRECTION ( 'NONE',  ( 0.000000000000000000, 0.000000000000000000, 1.000000000000000000 ) ) ;
#3705=EDGE_CURVE ( 'NONE', #1408, #1346, #683, .T. ) ;
#3710=CARTESIAN_POINT ( 'NONE',  ( 2.399999999999999911, 0.000000000000000000, 0.000000000000000000 ) ) ;
#3712=DIRECTION ( 'NONE',  ( 0.000000000000000000, 0.000000000000000000, -1.000000000000000000 ) ) ;
#3718=DIRECTION ( 'NONE',  ( 0.000000000000000000, 0.000000000000000000, 1.000000000000000000 ) ) ;
#3723=DIRECTION ( 'NONE',  ( 0.000000000000000000, 1.000000000000000000, 1.224646799147353454E-16 ) ) ;
#3726=ORIENTED_EDGE ( 'NONE', *, *, #1827, .F. ) ;
#3730=EDGE_CURVE ( 'NONE', #1813, #2170, #2028, .T. ) ;
#3732=ORIENTED_EDGE ( 'NONE', *, *, #1051, .F. ) ;
#3734=DIRECTION ( 'NONE',  ( 0.000000000000000000, 0.000000000000000000, 1.000000000000000000 ) ) ;
#3736=EDGE_CURVE ( 'NONE', #1528, #3430, #3030, .T. ) ;
#3739=DIRECTION ( 'NONE',  ( 0.000000000000000000, 0.000000000000000000, 1.000000000000000000 ) ) ;
#3740=DIRECTION ( 'NONE',  ( 0.000000000000000000, 0.000000000000000000, 1.000000000000000000 ) ) ;
#3748=ORIENTED_EDGE ( 'NONE', *, *, #564, .T. ) ;
#3757=ORIENTED_EDGE ( 'NONE', *, *, #2019, .T. ) ;
#3767=VECTOR ( 'NONE', #2429, 1000.000000000000114 ) ;
#3768=ORIENTED_EDGE ( 'NONE', *, *, #562, .T. ) ;
#3771=AXIS2_PLACEMENT_3D ( 'NONE', #1553, #3085, #2768 ) ;
#3775=ORIENTED_EDGE ( 'NONE', *, *, #564, .F. ) ;
#3778=EDGE_CURVE ( 'NONE', #2365, #2698, #333, .T. ) ;
#3787=ORIENTED_EDGE ( 'NONE', *, *, #2019, .F. ) ;
#3793=LINE ( 'NONE', #1730, #2405 ) ;
#3795=( LENGTH_UNIT ( ) NAMED_UNIT ( * ) SI_UNIT ( .MILLI., .METRE. ) );
#3797=ORIENTED_EDGE ( 'NONE', *, *, #1410, .F. ) ;
#3798=CARTESIAN_POINT ( 'NONE',  ( 2.021687836487040535, 2.168404344971008868E-16, 0.000000000000000000 ) ) ;
#3805=CARTESIAN_POINT ( 'NONE',  ( 2.399999999999999911, 0.000000000000000000, 2.199999999999999289 ) ) ;
#3806=PLANE ( 'NONE',  #895 ) ;
#3812=AXIS2_PLACEMENT_3D ( 'NONE', #2432, #1865, #1250 ) ;
#3814=ORIENTED_EDGE ( 'NONE', *, *, #1785, .T. ) ;
#3818=CARTESIAN_POINT ( 'NONE',  ( 1.820000000000000062, 0.000000000000000000, 0.000000000000000000 ) ) ;
#3819=ORIENTED_EDGE ( 'NONE', *, *, #1785, .F. ) ;
#3821=VECTOR ( 'NONE', #3060, 1000.000000000000000 ) ;
#3823=CARTESIAN_POINT ( 'NONE',  ( 1.300000000000000044, -0.7216878364870317197, 1.250000000000000000 ) ) ;
#3828=AXIS2_PLACEMENT_3D ( 'NONE', #1968, #2260, #2317 ) ;
#3834=( NAMED_UNIT ( * ) PLANE_ANGLE_UNIT ( ) SI_UNIT ( $, .RADIAN. ) );
#3835=ORIENTED_EDGE ( 'NONE', *, *, #2388, .F. ) ;
#3875=COLOUR_RGB('Black',0.12,0.14,0.17);
#3876=FILL_AREA_STYLE_COLOUR('',#3875);
#3877=FILL_AREA_STYLE('',(#3876));
#3878=SURFACE_STYLE_FILL_AREA(#3877);
#3879=SURFACE_SIDE_STYLE('',(#3878));
#3880=SURFACE_STYLE_USAGE(.BOTH.,#3879);
#3881=PRESENTATION_STYLE_ASSIGNMENT((#3880));
ENDSEC;
END-ISO-10303-21;
